ISO-10303-21;
HEADER;
/* Generated by software containing ST-Developer
 * from STEP Tools, Inc. (www.steptools.com) 
 */

FILE_DESCRIPTION(
/* description */ ('Hand-crank gear train demonstrator'),
/* implementation_level */ '2;1');

FILE_NAME(
/* name */ 'M4x30 post bolt.step',
/* time_stamp */ '2026-10-28T03:22:13-07:00',
/* author */ (''),
/* organization */ (''),
/* preprocessor_version */ 'ST-DEVELOPER v20.2',
/* originating_system */ 'Autodesk Translation Framework v15.17.0.0',
/* authorisation */ '');

FILE_SCHEMA (('AUTOMOTIVE_DESIGN { 1 0 10303 214 3 1 1 }'));
ENDSEC;

DATA;
#10=MECHANICAL_DESIGN_GEOMETRIC_PRESENTATION_REPRESENTATION('',(#1231),#62758);
#1039=CONICAL_SURFACE('',#17961,0.325,0.785398163397448);
#1040=CONICAL_SURFACE('',#17965,0.335,0.785398163397448);
#1041=CONICAL_SURFACE('',#17969,0.21,0.463647609000806);
#1053=ORIENTED_CLOSED_SHELL('',*,#16413,.F.);
#1058=BREP_WITH_VOIDS('Body1',#16414,(#1053));
#1088=SHAPE_REPRESENTATION_RELATIONSHIP('SRR','None',#63062,#1152);
#1152=ADVANCED_BREP_SHAPE_REPRESENTATION('',(#1058),#62716);
#1231=STYLED_ITEM('',(#63469),#1058);
#1540=FACE_BOUND('',#3672,.T.);
#1541=FACE_BOUND('',#3680,.T.);
#1871=PLANE('',#17945);
#1872=PLANE('',#17946);
#1873=PLANE('',#17947);
#1874=PLANE('',#17948);
#1875=PLANE('',#17949);
#1876=PLANE('',#17950);
#1877=PLANE('',#17951);
#1878=PLANE('',#17952);
#1879=PLANE('',#17953);
#1880=PLANE('',#17958);
#1881=PLANE('',#17959);
#1882=PLANE('',#17967);
#2529=FACE_OUTER_BOUND('',#3663,.T.);
#2530=FACE_OUTER_BOUND('',#3664,.T.);
#2531=FACE_OUTER_BOUND('',#3665,.T.);
#2532=FACE_OUTER_BOUND('',#3666,.T.);
#2533=FACE_OUTER_BOUND('',#3667,.T.);
#2534=FACE_OUTER_BOUND('',#3668,.T.);
#2535=FACE_OUTER_BOUND('',#3669,.T.);
#2536=FACE_OUTER_BOUND('',#3670,.T.);
#2537=FACE_OUTER_BOUND('',#3671,.T.);
#2538=FACE_OUTER_BOUND('',#3673,.T.);
#2539=FACE_OUTER_BOUND('',#3674,.T.);
#2540=FACE_OUTER_BOUND('',#3675,.T.);
#2541=FACE_OUTER_BOUND('',#3676,.T.);
#2542=FACE_OUTER_BOUND('',#3677,.T.);
#2543=FACE_OUTER_BOUND('',#3678,.T.);
#2544=FACE_OUTER_BOUND('',#3679,.T.);
#2545=FACE_OUTER_BOUND('',#3681,.T.);
#2546=FACE_OUTER_BOUND('',#3682,.T.);
#3663=EDGE_LOOP('',(#12643,#12644,#12645,#12646));
#3664=EDGE_LOOP('',(#12647,#12648,#12649,#12650));
#3665=EDGE_LOOP('',(#12651,#12652,#12653,#12654));
#3666=EDGE_LOOP('',(#12655,#12656,#12657,#12658));
#3667=EDGE_LOOP('',(#12659,#12660,#12661,#12662));
#3668=EDGE_LOOP('',(#12663,#12664,#12665,#12666));
#3669=EDGE_LOOP('',(#12667,#12668,#12669,#12670,#12671,#12672));
#3670=EDGE_LOOP('',(#12673,#12674,#12675,#12676,#12677,#12678));
#3671=EDGE_LOOP('',(#12679));
#3672=EDGE_LOOP('',(#12680));
#3673=EDGE_LOOP('',(#12681,#12682,#12683,#12684));
#3674=EDGE_LOOP('',(#12685));
#3675=EDGE_LOOP('',(#12686));
#3676=EDGE_LOOP('',(#12687,#12688,#12689,#12690));
#3677=EDGE_LOOP('',(#12691,#12692,#12693,#12694));
#3678=EDGE_LOOP('',(#12695,#12696,#12697,#12698));
#3679=EDGE_LOOP('',(#12699));
#3680=EDGE_LOOP('',(#12700));
#3681=EDGE_LOOP('',(#12701,#12702,#12703,#12704));
#3682=EDGE_LOOP('',(#12705,#12706,#12707,#12708));
#4819=LINE('',#25914,#5951);
#4820=LINE('',#25916,#5952);
#4821=LINE('',#25918,#5953);
#4822=LINE('',#25919,#5954);
#4823=LINE('',#25922,#5955);
#4824=LINE('',#25924,#5956);
#4825=LINE('',#25925,#5957);
#4826=LINE('',#25928,#5958);
#4827=LINE('',#25930,#5959);
#4828=LINE('',#25931,#5960);
#4829=LINE('',#25934,#5961);
#4830=LINE('',#25936,#5962);
#4831=LINE('',#25937,#5963);
#4832=LINE('',#25940,#5964);
#4833=LINE('',#25942,#5965);
#4834=LINE('',#25943,#5966);
#4835=LINE('',#25945,#5967);
#4836=LINE('',#25946,#5968);
#4837=LINE('',#25956,#5969);
#4838=LINE('',#25965,#5970);
#4839=LINE('',#25969,#5971);
#4840=LINE('',#25973,#5972);
#4841=LINE('',#25980,#5973);
#4842=LINE('',#25982,#5974);
#5951=VECTOR('',#20940,1.);
#5952=VECTOR('',#20941,1.);
#5953=VECTOR('',#20942,1.);
#5954=VECTOR('',#20943,1.);
#5955=VECTOR('',#20946,1.);
#5956=VECTOR('',#20947,1.);
#5957=VECTOR('',#20948,1.);
#5958=VECTOR('',#20951,1.);
#5959=VECTOR('',#20952,1.);
#5960=VECTOR('',#20953,1.);
#5961=VECTOR('',#20956,1.);
#5962=VECTOR('',#20957,1.);
#5963=VECTOR('',#20958,1.);
#5964=VECTOR('',#20961,1.);
#5965=VECTOR('',#20962,1.);
#5966=VECTOR('',#20963,1.);
#5967=VECTOR('',#20966,1.);
#5968=VECTOR('',#20967,1.);
#5969=VECTOR('',#20980,0.2);
#5970=VECTOR('',#20993,0.325);
#5971=VECTOR('',#20998,0.35);
#5972=VECTOR('',#21003,0.335);
#5973=VECTOR('',#21012,0.21);
#5974=VECTOR('',#21015,0.2);
#6889=CIRCLE('',#17954,0.2);
#6890=CIRCLE('',#17955,0.1954);
#6891=CIRCLE('',#17957,0.2);
#6892=CIRCLE('',#17960,0.3);
#6893=CIRCLE('',#17962,0.35);
#6894=CIRCLE('',#17964,0.35);
#6895=CIRCLE('',#17966,0.32);
#6896=CIRCLE('',#17968,0.22);
#6897=CIRCLE('',#17970,0.1954);
#7830=VERTEX_POINT('',#25912);
#7831=VERTEX_POINT('',#25913);
#7832=VERTEX_POINT('',#25915);
#7833=VERTEX_POINT('',#25917);
#7834=VERTEX_POINT('',#25921);
#7835=VERTEX_POINT('',#25923);
#7836=VERTEX_POINT('',#25927);
#7837=VERTEX_POINT('',#25929);
#7838=VERTEX_POINT('',#25933);
#7839=VERTEX_POINT('',#25935);
#7840=VERTEX_POINT('',#25939);
#7841=VERTEX_POINT('',#25941);
#7842=VERTEX_POINT('',#25950);
#7843=VERTEX_POINT('',#25952);
#7844=VERTEX_POINT('',#25955);
#7845=VERTEX_POINT('',#25960);
#7846=VERTEX_POINT('',#25963);
#7847=VERTEX_POINT('',#25967);
#7848=VERTEX_POINT('',#25971);
#7849=VERTEX_POINT('',#25975);
#7850=VERTEX_POINT('',#25978);
#9573=EDGE_CURVE('',#7830,#7831,#4819,.T.);
#9574=EDGE_CURVE('',#7831,#7832,#4820,.T.);
#9575=EDGE_CURVE('',#7832,#7833,#4821,.T.);
#9576=EDGE_CURVE('',#7830,#7833,#4822,.T.);
#9577=EDGE_CURVE('',#7831,#7834,#4823,.T.);
#9578=EDGE_CURVE('',#7834,#7835,#4824,.T.);
#9579=EDGE_CURVE('',#7835,#7832,#4825,.T.);
#9580=EDGE_CURVE('',#7834,#7836,#4826,.T.);
#9581=EDGE_CURVE('',#7836,#7837,#4827,.T.);
#9582=EDGE_CURVE('',#7837,#7835,#4828,.T.);
#9583=EDGE_CURVE('',#7836,#7838,#4829,.T.);
#9584=EDGE_CURVE('',#7838,#7839,#4830,.T.);
#9585=EDGE_CURVE('',#7839,#7837,#4831,.T.);
#9586=EDGE_CURVE('',#7838,#7840,#4832,.T.);
#9587=EDGE_CURVE('',#7840,#7841,#4833,.T.);
#9588=EDGE_CURVE('',#7841,#7839,#4834,.T.);
#9589=EDGE_CURVE('',#7840,#7830,#4835,.T.);
#9590=EDGE_CURVE('',#7833,#7841,#4836,.T.);
#9591=EDGE_CURVE('',#7842,#7842,#6889,.T.);
#9592=EDGE_CURVE('',#7843,#7843,#6890,.T.);
#9593=EDGE_CURVE('',#7842,#7844,#4837,.T.);
#9594=EDGE_CURVE('',#7844,#7844,#6891,.T.);
#9595=EDGE_CURVE('',#7845,#7845,#6892,.T.);
#9596=EDGE_CURVE('',#7846,#7846,#6893,.T.);
#9597=EDGE_CURVE('',#7846,#7845,#4838,.T.);
#9598=EDGE_CURVE('',#7847,#7847,#6894,.T.);
#9599=EDGE_CURVE('',#7847,#7846,#4839,.T.);
#9600=EDGE_CURVE('',#7848,#7848,#6895,.T.);
#9601=EDGE_CURVE('',#7848,#7847,#4840,.T.);
#9602=EDGE_CURVE('',#7849,#7849,#6896,.T.);
#9603=EDGE_CURVE('',#7850,#7850,#6897,.F.);
#9604=EDGE_CURVE('',#7850,#7849,#4841,.T.);
#9605=EDGE_CURVE('',#7843,#7850,#4842,.T.);
#12643=ORIENTED_EDGE('',*,*,#9573,.T.);
#12644=ORIENTED_EDGE('',*,*,#9574,.T.);
#12645=ORIENTED_EDGE('',*,*,#9575,.T.);
#12646=ORIENTED_EDGE('',*,*,#9576,.F.);
#12647=ORIENTED_EDGE('',*,*,#9577,.T.);
#12648=ORIENTED_EDGE('',*,*,#9578,.T.);
#12649=ORIENTED_EDGE('',*,*,#9579,.T.);
#12650=ORIENTED_EDGE('',*,*,#9574,.F.);
#12651=ORIENTED_EDGE('',*,*,#9580,.T.);
#12652=ORIENTED_EDGE('',*,*,#9581,.T.);
#12653=ORIENTED_EDGE('',*,*,#9582,.T.);
#12654=ORIENTED_EDGE('',*,*,#9578,.F.);
#12655=ORIENTED_EDGE('',*,*,#9583,.T.);
#12656=ORIENTED_EDGE('',*,*,#9584,.T.);
#12657=ORIENTED_EDGE('',*,*,#9585,.T.);
#12658=ORIENTED_EDGE('',*,*,#9581,.F.);
#12659=ORIENTED_EDGE('',*,*,#9586,.T.);
#12660=ORIENTED_EDGE('',*,*,#9587,.T.);
#12661=ORIENTED_EDGE('',*,*,#9588,.T.);
#12662=ORIENTED_EDGE('',*,*,#9584,.F.);
#12663=ORIENTED_EDGE('',*,*,#9589,.T.);
#12664=ORIENTED_EDGE('',*,*,#9576,.T.);
#12665=ORIENTED_EDGE('',*,*,#9590,.T.);
#12666=ORIENTED_EDGE('',*,*,#9587,.F.);
#12667=ORIENTED_EDGE('',*,*,#9589,.F.);
#12668=ORIENTED_EDGE('',*,*,#9586,.F.);
#12669=ORIENTED_EDGE('',*,*,#9583,.F.);
#12670=ORIENTED_EDGE('',*,*,#9580,.F.);
#12671=ORIENTED_EDGE('',*,*,#9577,.F.);
#12672=ORIENTED_EDGE('',*,*,#9573,.F.);
#12673=ORIENTED_EDGE('',*,*,#9590,.F.);
#12674=ORIENTED_EDGE('',*,*,#9575,.F.);
#12675=ORIENTED_EDGE('',*,*,#9579,.F.);
#12676=ORIENTED_EDGE('',*,*,#9582,.F.);
#12677=ORIENTED_EDGE('',*,*,#9585,.F.);
#12678=ORIENTED_EDGE('',*,*,#9588,.F.);
#12679=ORIENTED_EDGE('',*,*,#9591,.T.);
#12680=ORIENTED_EDGE('',*,*,#9592,.F.);
#12681=ORIENTED_EDGE('',*,*,#9591,.F.);
#12682=ORIENTED_EDGE('',*,*,#9593,.T.);
#12683=ORIENTED_EDGE('',*,*,#9594,.T.);
#12684=ORIENTED_EDGE('',*,*,#9593,.F.);
#12685=ORIENTED_EDGE('',*,*,#9594,.F.);
#12686=ORIENTED_EDGE('',*,*,#9595,.F.);
#12687=ORIENTED_EDGE('',*,*,#9596,.F.);
#12688=ORIENTED_EDGE('',*,*,#9597,.T.);
#12689=ORIENTED_EDGE('',*,*,#9595,.T.);
#12690=ORIENTED_EDGE('',*,*,#9597,.F.);
#12691=ORIENTED_EDGE('',*,*,#9598,.F.);
#12692=ORIENTED_EDGE('',*,*,#9599,.T.);
#12693=ORIENTED_EDGE('',*,*,#9596,.T.);
#12694=ORIENTED_EDGE('',*,*,#9599,.F.);
#12695=ORIENTED_EDGE('',*,*,#9600,.F.);
#12696=ORIENTED_EDGE('',*,*,#9601,.T.);
#12697=ORIENTED_EDGE('',*,*,#9598,.T.);
#12698=ORIENTED_EDGE('',*,*,#9601,.F.);
#12699=ORIENTED_EDGE('',*,*,#9600,.T.);
#12700=ORIENTED_EDGE('',*,*,#9602,.F.);
#12701=ORIENTED_EDGE('',*,*,#9603,.F.);
#12702=ORIENTED_EDGE('',*,*,#9604,.T.);
#12703=ORIENTED_EDGE('',*,*,#9602,.T.);
#12704=ORIENTED_EDGE('',*,*,#9604,.F.);
#12705=ORIENTED_EDGE('',*,*,#9592,.T.);
#12706=ORIENTED_EDGE('',*,*,#9605,.T.);
#12707=ORIENTED_EDGE('',*,*,#9603,.T.);
#12708=ORIENTED_EDGE('',*,*,#9605,.F.);
#15287=CYLINDRICAL_SURFACE('',#17956,0.2);
#15288=CYLINDRICAL_SURFACE('',#17963,0.35);
#15289=CYLINDRICAL_SURFACE('',#17971,0.1954);
#15839=ADVANCED_FACE('',(#2529),#1871,.F.);
#15840=ADVANCED_FACE('',(#2530),#1872,.F.);
#15841=ADVANCED_FACE('',(#2531),#1873,.F.);
#15842=ADVANCED_FACE('',(#2532),#1874,.F.);
#15843=ADVANCED_FACE('',(#2533),#1875,.F.);
#15844=ADVANCED_FACE('',(#2534),#1876,.F.);
#15845=ADVANCED_FACE('',(#2535),#1877,.F.);
#15846=ADVANCED_FACE('',(#2536),#1878,.F.);
#15847=ADVANCED_FACE('',(#2537,#1540),#1879,.T.);
#15848=ADVANCED_FACE('',(#2538),#15287,.T.);
#15849=ADVANCED_FACE('',(#2539),#1880,.F.);
#15850=ADVANCED_FACE('',(#2540),#1881,.T.);
#15851=ADVANCED_FACE('',(#2541),#1039,.T.);
#15852=ADVANCED_FACE('',(#2542),#15288,.T.);
#15853=ADVANCED_FACE('',(#2543),#1040,.T.);
#15854=ADVANCED_FACE('',(#2544,#1541),#1882,.T.);
#15855=ADVANCED_FACE('',(#2545),#1041,.T.);
#15856=ADVANCED_FACE('',(#2546),#15289,.T.);
#16413=CLOSED_SHELL('',(#15839,#15840,#15841,#15842,#15843,#15844,#15845,
#15846));
#16414=CLOSED_SHELL('',(#15847,#15848,#15849,#15850,#15851,#15852,#15853,
#15854,#15855,#15856));
#17944=AXIS2_PLACEMENT_3D('',#25910,#20936,#20937);
#17945=AXIS2_PLACEMENT_3D('',#25911,#20938,#20939);
#17946=AXIS2_PLACEMENT_3D('',#25920,#20944,#20945);
#17947=AXIS2_PLACEMENT_3D('',#25926,#20949,#20950);
#17948=AXIS2_PLACEMENT_3D('',#25932,#20954,#20955);
#17949=AXIS2_PLACEMENT_3D('',#25938,#20959,#20960);
#17950=AXIS2_PLACEMENT_3D('',#25944,#20964,#20965);
#17951=AXIS2_PLACEMENT_3D('',#25947,#20968,#20969);
#17952=AXIS2_PLACEMENT_3D('',#25948,#20970,#20971);
#17953=AXIS2_PLACEMENT_3D('',#25949,#20972,#20973);
#17954=AXIS2_PLACEMENT_3D('',#25951,#20974,#20975);
#17955=AXIS2_PLACEMENT_3D('',#25953,#20976,#20977);
#17956=AXIS2_PLACEMENT_3D('',#25954,#20978,#20979);
#17957=AXIS2_PLACEMENT_3D('',#25957,#20981,#20982);
#17958=AXIS2_PLACEMENT_3D('',#25958,#20983,#20984);
#17959=AXIS2_PLACEMENT_3D('',#25959,#20985,#20986);
#17960=AXIS2_PLACEMENT_3D('',#25961,#20987,#20988);
#17961=AXIS2_PLACEMENT_3D('',#25962,#20989,#20990);
#17962=AXIS2_PLACEMENT_3D('',#25964,#20991,#20992);
#17963=AXIS2_PLACEMENT_3D('',#25966,#20994,#20995);
#17964=AXIS2_PLACEMENT_3D('',#25968,#20996,#20997);
#17965=AXIS2_PLACEMENT_3D('',#25970,#20999,#21000);
#17966=AXIS2_PLACEMENT_3D('',#25972,#21001,#21002);
#17967=AXIS2_PLACEMENT_3D('',#25974,#21004,#21005);
#17968=AXIS2_PLACEMENT_3D('',#25976,#21006,#21007);
#17969=AXIS2_PLACEMENT_3D('',#25977,#21008,#21009);
#17970=AXIS2_PLACEMENT_3D('',#25979,#21010,#21011);
#17971=AXIS2_PLACEMENT_3D('',#25981,#21013,#21014);
#20936=DIRECTION('axis',(0.,0.,1.));
#20937=DIRECTION('refdir',(1.,0.,0.));
#20938=DIRECTION('center_axis',(0.866025403784439,0.,-0.5));
#20939=DIRECTION('ref_axis',(0.5,0.,0.866025403784439));
#20940=DIRECTION('',(-0.5,0.,-0.866025403784439));
#20941=DIRECTION('',(0.,-1.,0.));
#20942=DIRECTION('',(0.5,0.,0.866025403784439));
#20943=DIRECTION('',(0.,-1.,0.));
#20944=DIRECTION('center_axis',(1.60246890531964E-16,0.,-1.));
#20945=DIRECTION('ref_axis',(1.,0.,1.60246890531964E-16));
#20946=DIRECTION('',(-1.,0.,-1.60246890531964E-16));
#20947=DIRECTION('',(0.,-1.,0.));
#20948=DIRECTION('',(1.,0.,1.60246890531964E-16));
#20949=DIRECTION('center_axis',(-0.866025403784439,0.,-0.5));
#20950=DIRECTION('ref_axis',(0.5,0.,-0.866025403784439));
#20951=DIRECTION('',(-0.5,0.,0.866025403784439));
#20952=DIRECTION('',(0.,-1.,0.));
#20953=DIRECTION('',(0.5,0.,-0.866025403784439));
#20954=DIRECTION('center_axis',(-0.866025403784439,0.,0.5));
#20955=DIRECTION('ref_axis',(-0.5,0.,-0.866025403784439));
#20956=DIRECTION('',(0.5,0.,0.866025403784439));
#20957=DIRECTION('',(0.,-1.,0.));
#20958=DIRECTION('',(-0.5,0.,-0.866025403784439));
#20959=DIRECTION('center_axis',(-1.60246890531964E-16,0.,1.));
#20960=DIRECTION('ref_axis',(-1.,0.,-1.60246890531964E-16));
#20961=DIRECTION('',(1.,0.,1.60246890531964E-16));
#20962=DIRECTION('',(0.,-1.,0.));
#20963=DIRECTION('',(-1.,0.,-1.60246890531964E-16));
#20964=DIRECTION('center_axis',(0.866025403784439,0.,0.5));
#20965=DIRECTION('ref_axis',(-0.5,0.,0.866025403784439));
#20966=DIRECTION('',(0.5,0.,-0.866025403784439));
#20967=DIRECTION('',(-0.5,0.,0.866025403784439));
#20968=DIRECTION('center_axis',(0.,1.,0.));
#20969=DIRECTION('ref_axis',(1.,0.,0.));
#20970=DIRECTION('center_axis',(0.,-1.,0.));
#20971=DIRECTION('ref_axis',(0.,0.,-1.));
#20972=DIRECTION('center_axis',(0.,1.,0.));
#20973=DIRECTION('ref_axis',(1.,0.,0.));
#20974=DIRECTION('center_axis',(0.,1.,0.));
#20975=DIRECTION('ref_axis',(1.,0.,0.));
#20976=DIRECTION('center_axis',(0.,1.,0.));
#20977=DIRECTION('ref_axis',(1.,0.,0.));
#20978=DIRECTION('center_axis',(0.,1.,0.));
#20979=DIRECTION('ref_axis',(1.,0.,0.));
#20980=DIRECTION('',(0.,-1.,0.));
#20981=DIRECTION('center_axis',(0.,1.,0.));
#20982=DIRECTION('ref_axis',(1.,0.,0.));
#20983=DIRECTION('center_axis',(0.,1.,0.));
#20984=DIRECTION('ref_axis',(1.,0.,0.));
#20985=DIRECTION('center_axis',(0.,1.,0.));
#20986=DIRECTION('ref_axis',(0.,0.,1.));
#20987=DIRECTION('center_axis',(0.,-1.,0.));
#20988=DIRECTION('ref_axis',(1.,0.,0.));
#20989=DIRECTION('center_axis',(0.,-1.,0.));
#20990=DIRECTION('ref_axis',(1.,0.,0.));
#20991=DIRECTION('center_axis',(0.,-1.,0.));
#20992=DIRECTION('ref_axis',(1.,0.,0.));
#20993=DIRECTION('',(0.707106781186547,0.707106781186548,8.65956056235493E-17));
#20994=DIRECTION('center_axis',(0.,-1.,0.));
#20995=DIRECTION('ref_axis',(1.,0.,0.));
#20996=DIRECTION('center_axis',(0.,-1.,0.));
#20997=DIRECTION('ref_axis',(1.,0.,0.));
#20998=DIRECTION('',(0.,1.,0.));
#20999=DIRECTION('center_axis',(0.,1.,0.));
#21000=DIRECTION('ref_axis',(1.,0.,0.));
#21001=DIRECTION('center_axis',(0.,-1.,0.));
#21002=DIRECTION('ref_axis',(1.,0.,0.));
#21003=DIRECTION('',(-0.707106781186547,0.707106781186548,-8.65956056235493E-17));
#21004=DIRECTION('center_axis',(0.,-1.,0.));
#21005=DIRECTION('ref_axis',(0.,0.,-1.));
#21006=DIRECTION('center_axis',(0.,-1.,0.));
#21007=DIRECTION('ref_axis',(1.,0.,0.));
#21008=DIRECTION('center_axis',(0.,1.,0.));
#21009=DIRECTION('ref_axis',(1.,0.,0.));
#21010=DIRECTION('center_axis',(0.,1.,0.));
#21011=DIRECTION('ref_axis',(1.,0.,0.));
#21012=DIRECTION('',(-0.447213595499958,0.894427190999916,-5.47678698264203E-17));
#21013=DIRECTION('center_axis',(0.,-1.,0.));
#21014=DIRECTION('ref_axis',(1.,0.,0.));
#21015=DIRECTION('',(0.,1.,0.));
#25910=CARTESIAN_POINT('',(0.,0.,0.));
#25911=CARTESIAN_POINT('Origin',(0.0866025403784439,-0.4,-0.15));
#25912=CARTESIAN_POINT('',(0.173205080756888,-0.4,0.));
#25913=CARTESIAN_POINT('',(0.0866025403784439,-0.4,-0.15));
#25914=CARTESIAN_POINT('',(0.173205080756888,-0.4,0.));
#25915=CARTESIAN_POINT('',(0.0866025403784439,-0.64,-0.15));
#25916=CARTESIAN_POINT('',(0.0866025403784439,-0.4,-0.15));
#25917=CARTESIAN_POINT('',(0.173205080756888,-0.64,0.));
#25918=CARTESIAN_POINT('',(0.173205080756888,-0.64,0.));
#25919=CARTESIAN_POINT('',(0.173205080756888,-0.4,0.));
#25920=CARTESIAN_POINT('Origin',(-0.0866025403784438,-0.4,-0.15));
#25921=CARTESIAN_POINT('',(-0.0866025403784438,-0.4,-0.15));
#25922=CARTESIAN_POINT('',(0.0866025403784439,-0.4,-0.15));
#25923=CARTESIAN_POINT('',(-0.0866025403784438,-0.64,-0.15));
#25924=CARTESIAN_POINT('',(-0.0866025403784438,-0.4,-0.15));
#25925=CARTESIAN_POINT('',(0.0866025403784439,-0.64,-0.15));
#25926=CARTESIAN_POINT('Origin',(-0.173205080756888,-0.4,-2.77555756156289E-17));
#25927=CARTESIAN_POINT('',(-0.173205080756888,-0.4,-2.12115047744981E-17));
#25928=CARTESIAN_POINT('',(-0.0866025403784438,-0.4,-0.15));
#25929=CARTESIAN_POINT('',(-0.173205080756888,-0.64,-2.77555756156289E-17));
#25930=CARTESIAN_POINT('',(-0.173205080756888,-0.4,-2.12115047744981E-17));
#25931=CARTESIAN_POINT('',(-0.0866025403784438,-0.64,-0.15));
#25932=CARTESIAN_POINT('Origin',(-0.0866025403784439,-0.4,0.15));
#25933=CARTESIAN_POINT('',(-0.0866025403784439,-0.4,0.15));
#25934=CARTESIAN_POINT('',(-0.173205080756888,-0.4,-2.12115047744981E-17));
#25935=CARTESIAN_POINT('',(-0.0866025403784439,-0.64,0.15));
#25936=CARTESIAN_POINT('',(-0.0866025403784439,-0.4,0.15));
#25937=CARTESIAN_POINT('',(-0.173205080756888,-0.64,-2.12115047744981E-17));
#25938=CARTESIAN_POINT('Origin',(0.0866025403784439,-0.4,0.15));
#25939=CARTESIAN_POINT('',(0.0866025403784439,-0.4,0.15));
#25940=CARTESIAN_POINT('',(-0.0866025403784439,-0.4,0.15));
#25941=CARTESIAN_POINT('',(0.0866025403784439,-0.64,0.15));
#25942=CARTESIAN_POINT('',(0.0866025403784439,-0.4,0.15));
#25943=CARTESIAN_POINT('',(-0.0866025403784439,-0.64,0.15));
#25944=CARTESIAN_POINT('Origin',(0.173205080756888,-0.4,0.));
#25945=CARTESIAN_POINT('',(0.0866025403784439,-0.4,0.15));
#25946=CARTESIAN_POINT('',(0.0866025403784439,-0.64,0.15));
#25947=CARTESIAN_POINT('Origin',(0.,-0.4,-2.77555756156289E-17));
#25948=CARTESIAN_POINT('Origin',(0.,-0.64,-2.77555756156289E-17));
#25949=CARTESIAN_POINT('Origin',(0.,-1.5,0.));
#25950=CARTESIAN_POINT('',(-0.2,-1.5,2.44929359829471E-17));
#25951=CARTESIAN_POINT('Origin',(0.,-1.5,0.));
#25952=CARTESIAN_POINT('',(-0.1954,-1.5,2.39295984553393E-17));
#25953=CARTESIAN_POINT('Origin',(0.,-1.5,0.));
#25954=CARTESIAN_POINT('Origin',(0.,-3.,0.));
#25955=CARTESIAN_POINT('',(-0.2,-3.,2.44929359829471E-17));
#25956=CARTESIAN_POINT('',(-0.2,-3.,2.44929359829471E-17));
#25957=CARTESIAN_POINT('Origin',(0.,-3.,0.));
#25958=CARTESIAN_POINT('Origin',(0.,-3.,0.));
#25959=CARTESIAN_POINT('Origin',(0.3,0.4,0.));
#25960=CARTESIAN_POINT('',(-0.3,0.4,-3.67394039744206E-17));
#25961=CARTESIAN_POINT('Origin',(0.,0.4,0.));
#25962=CARTESIAN_POINT('Origin',(0.,0.375,0.));
#25963=CARTESIAN_POINT('',(-0.35,0.35,-4.28626379701573E-17));
#25964=CARTESIAN_POINT('Origin',(0.,0.35,0.));
#25965=CARTESIAN_POINT('',(-0.325,0.375,-3.9801020972289E-17));
#25966=CARTESIAN_POINT('Origin',(0.,0.19,0.));
#25967=CARTESIAN_POINT('',(-0.35,0.03,-4.28626379701574E-17));
#25968=CARTESIAN_POINT('Origin',(0.,0.03,0.));
#25969=CARTESIAN_POINT('',(-0.35,0.19,-4.28626379701574E-17));
#25970=CARTESIAN_POINT('Origin',(0.,0.0149999999999999,0.));
#25971=CARTESIAN_POINT('',(-0.32,-3.29597460435593E-17,-3.91886975727153E-17));
#25972=CARTESIAN_POINT('Origin',(0.,0.,0.));
#25973=CARTESIAN_POINT('',(-0.335,0.0149999999999999,-4.10256677714363E-17));
#25974=CARTESIAN_POINT('Origin',(0.22,0.,0.));
#25975=CARTESIAN_POINT('',(-0.22,-6.93889390390723E-18,-2.69422295812418E-17));
#25976=CARTESIAN_POINT('Origin',(0.,0.,0.));
#25977=CARTESIAN_POINT('Origin',(0.,-0.02,0.));
#25978=CARTESIAN_POINT('',(-0.1954,-0.0492,2.39295984553393E-17));
#25979=CARTESIAN_POINT('Origin',(0.,-0.0492,0.));
#25980=CARTESIAN_POINT('',(-0.21,-0.02,-2.57175827820944E-17));
#25981=CARTESIAN_POINT('Origin',(0.,-0.8,0.));
#25982=CARTESIAN_POINT('',(-0.1954,-0.8,-2.39295984553393E-17));
#62642=UNCERTAINTY_MEASURE_WITH_UNIT(LENGTH_MEASURE(0.001),#62759,
'DISTANCE_ACCURACY_VALUE',
'Maximum model space distance between geometric entities at asserted c
onnectivities');
#62684=UNCERTAINTY_MEASURE_WITH_UNIT(LENGTH_MEASURE(0.001),#62759,
'DISTANCE_ACCURACY_VALUE',
'Maximum model space distance between geometric entities at asserted c
onnectivities');
#62716=(
GEOMETRIC_REPRESENTATION_CONTEXT(3)
GLOBAL_UNCERTAINTY_ASSIGNED_CONTEXT((#62642))
GLOBAL_UNIT_ASSIGNED_CONTEXT((#62759,#62761,#62762))
REPRESENTATION_CONTEXT('','3D')
);
#62758=(
GEOMETRIC_REPRESENTATION_CONTEXT(3)
GLOBAL_UNCERTAINTY_ASSIGNED_CONTEXT((#62684))
GLOBAL_UNIT_ASSIGNED_CONTEXT((#62759,#62761,#62762))
REPRESENTATION_CONTEXT('','3D')
);
#62759=(
LENGTH_UNIT()
NAMED_UNIT(*)
SI_UNIT(.CENTI.,.METRE.)
);
#62761=(
NAMED_UNIT(*)
PLANE_ANGLE_UNIT()
SI_UNIT($,.RADIAN.)
);
#62762=(
NAMED_UNIT(*)
SI_UNIT($,.STERADIAN.)
SOLID_ANGLE_UNIT()
);
#62794=SHAPE_DEFINITION_REPRESENTATION(#62877,#63062);
#62877=PRODUCT_DEFINITION_SHAPE('',$,#63136);
#63062=SHAPE_REPRESENTATION('',(#17944),#62716);
#63104=PRODUCT_DEFINITION_CONTEXT('part definition',#63325,'design');
#63136=PRODUCT_DEFINITION('M4x30 post bolt','M4x30 post bolt',#63209,#63104);
#63209=PRODUCT_DEFINITION_FORMATION('',$,#63358);
#63325=APPLICATION_CONTEXT(
'Core Data for Automotive Mechanical Design Process');
#63326=PRODUCT_CONTEXT('part definition',#63325,'mechanical');
#63358=PRODUCT('M4x30 post bolt','M4x30 post bolt','M4x30 post bolt',(#63326));
#63463=COLOUR_RGB('Black',0.12,0.14,0.17);
#63464=FILL_AREA_STYLE_COLOUR('',#63463);
#63465=FILL_AREA_STYLE('',(#63464));
#63466=SURFACE_STYLE_FILL_AREA(#63465);
#63467=SURFACE_SIDE_STYLE('',(#63466));
#63468=SURFACE_STYLE_USAGE(.BOTH.,#63467);
#63469=PRESENTATION_STYLE_ASSIGNMENT((#63468));
ENDSEC;
END-ISO-10303-21;
